ISO-10303-21;
HEADER;
/* Generated by software containing ST-Developer
 * from STEP Tools, Inc. (www.steptools.com) 
 */

FILE_DESCRIPTION(
/* description */ ('Flange-mounted spindle'),
/* implementation_level */ '2;1');

FILE_NAME(
/* name */ 'Socket Set Screw - M5x8.step',
/* time_stamp */ '2026-10-27T10:49:51-07:00',
/* author */ (''),
/* organization */ (''),
/* preprocessor_version */ 'ST-DEVELOPER v20.2',
/* originating_system */ 'Autodesk Translation Framework v15.17.0.0',
/* authorisation */ '');

FILE_SCHEMA (('AUTOMOTIVE_DESIGN { 1 0 10303 214 3 1 1 }'));
ENDSEC;

DATA;
#10=MECHANICAL_DESIGN_GEOMETRIC_PRESENTATION_REPRESENTATION('',(#362),#11764);
#274=CONICAL_SURFACE('',#7120,0.235,0.785398163397448);
#275=CONICAL_SURFACE('',#7124,0.2125,0.785398163397448);
#307=SHAPE_REPRESENTATION_RELATIONSHIP('SRR','None',#11905,#334);
#334=ADVANCED_BREP_SHAPE_REPRESENTATION('',(#387),#11760);
#362=STYLED_ITEM('',(#12106),#387);
#387=MANIFOLD_SOLID_BREP('Body1',#6157);
#501=FACE_BOUND('',#1445,.T.);
#645=PLANE('',#7111);
#646=PLANE('',#7112);
#647=PLANE('',#7113);
#648=PLANE('',#7114);
#649=PLANE('',#7115);
#650=PLANE('',#7116);
#651=PLANE('',#7117);
#652=PLANE('',#7118);
#653=PLANE('',#7126);
#982=FACE_OUTER_BOUND('',#1437,.T.);
#983=FACE_OUTER_BOUND('',#1438,.T.);
#984=FACE_OUTER_BOUND('',#1439,.T.);
#985=FACE_OUTER_BOUND('',#1440,.T.);
#986=FACE_OUTER_BOUND('',#1441,.T.);
#987=FACE_OUTER_BOUND('',#1442,.T.);
#988=FACE_OUTER_BOUND('',#1443,.T.);
#989=FACE_OUTER_BOUND('',#1444,.T.);
#990=FACE_OUTER_BOUND('',#1446,.T.);
#991=FACE_OUTER_BOUND('',#1447,.T.);
#992=FACE_OUTER_BOUND('',#1448,.T.);
#993=FACE_OUTER_BOUND('',#1449,.T.);
#1437=EDGE_LOOP('',(#5465,#5466,#5467,#5468));
#1438=EDGE_LOOP('',(#5469,#5470,#5471,#5472));
#1439=EDGE_LOOP('',(#5473,#5474,#5475,#5476));
#1440=EDGE_LOOP('',(#5477,#5478,#5479,#5480));
#1441=EDGE_LOOP('',(#5481,#5482,#5483,#5484));
#1442=EDGE_LOOP('',(#5485,#5486,#5487,#5488));
#1443=EDGE_LOOP('',(#5489,#5490,#5491,#5492,#5493,#5494));
#1444=EDGE_LOOP('',(#5495));
#1445=EDGE_LOOP('',(#5496,#5497,#5498,#5499,#5500,#5501));
#1446=EDGE_LOOP('',(#5502,#5503,#5504,#5505));
#1447=EDGE_LOOP('',(#5506,#5507,#5508,#5509));
#1448=EDGE_LOOP('',(#5510,#5511,#5512,#5513));
#1449=EDGE_LOOP('',(#5514));
#1845=LINE('',#11463,#2267);
#1846=LINE('',#11465,#2268);
#1847=LINE('',#11467,#2269);
#1848=LINE('',#11468,#2270);
#1849=LINE('',#11471,#2271);
#1850=LINE('',#11473,#2272);
#1851=LINE('',#11474,#2273);
#1852=LINE('',#11477,#2274);
#1853=LINE('',#11479,#2275);
#1854=LINE('',#11480,#2276);
#1855=LINE('',#11483,#2277);
#1856=LINE('',#11485,#2278);
#1857=LINE('',#11486,#2279);
#1858=LINE('',#11489,#2280);
#1859=LINE('',#11491,#2281);
#1860=LINE('',#11492,#2282);
#1861=LINE('',#11494,#2283);
#1862=LINE('',#11495,#2284);
#1863=LINE('',#11503,#2285);
#1864=LINE('',#11507,#2286);
#1865=LINE('',#11511,#2287);
#2267=VECTOR('',#8880,1.);
#2268=VECTOR('',#8881,1.);
#2269=VECTOR('',#8882,1.);
#2270=VECTOR('',#8883,1.);
#2271=VECTOR('',#8886,1.);
#2272=VECTOR('',#8887,1.);
#2273=VECTOR('',#8888,1.);
#2274=VECTOR('',#8891,1.);
#2275=VECTOR('',#8892,1.);
#2276=VECTOR('',#8893,1.);
#2277=VECTOR('',#8896,1.);
#2278=VECTOR('',#8897,1.);
#2279=VECTOR('',#8898,1.);
#2280=VECTOR('',#8901,1.);
#2281=VECTOR('',#8902,1.);
#2282=VECTOR('',#8903,1.);
#2283=VECTOR('',#8906,1.);
#2284=VECTOR('',#8907,1.);
#2285=VECTOR('',#8918,0.235);
#2286=VECTOR('',#8923,0.25);
#2287=VECTOR('',#8928,0.2125);
#2637=CIRCLE('',#7119,0.22);
#2638=CIRCLE('',#7121,0.24505);
#2639=CIRCLE('',#7123,0.24505);
#2640=CIRCLE('',#7125,0.175);
#3143=VERTEX_POINT('',#11461);
#3144=VERTEX_POINT('',#11462);
#3145=VERTEX_POINT('',#11464);
#3146=VERTEX_POINT('',#11466);
#3147=VERTEX_POINT('',#11470);
#3148=VERTEX_POINT('',#11472);
#3149=VERTEX_POINT('',#11476);
#3150=VERTEX_POINT('',#11478);
#3151=VERTEX_POINT('',#11482);
#3152=VERTEX_POINT('',#11484);
#3153=VERTEX_POINT('',#11488);
#3154=VERTEX_POINT('',#11490);
#3155=VERTEX_POINT('',#11498);
#3156=VERTEX_POINT('',#11501);
#3157=VERTEX_POINT('',#11505);
#3158=VERTEX_POINT('',#11509);
#3925=EDGE_CURVE('',#3143,#3144,#1845,.T.);
#3926=EDGE_CURVE('',#3143,#3145,#1846,.T.);
#3927=EDGE_CURVE('',#3145,#3146,#1847,.T.);
#3928=EDGE_CURVE('',#3144,#3146,#1848,.T.);
#3929=EDGE_CURVE('',#3147,#3143,#1849,.T.);
#3930=EDGE_CURVE('',#3147,#3148,#1850,.T.);
#3931=EDGE_CURVE('',#3148,#3145,#1851,.T.);
#3932=EDGE_CURVE('',#3149,#3147,#1852,.T.);
#3933=EDGE_CURVE('',#3149,#3150,#1853,.T.);
#3934=EDGE_CURVE('',#3150,#3148,#1854,.T.);
#3935=EDGE_CURVE('',#3151,#3149,#1855,.T.);
#3936=EDGE_CURVE('',#3151,#3152,#1856,.T.);
#3937=EDGE_CURVE('',#3152,#3150,#1857,.T.);
#3938=EDGE_CURVE('',#3153,#3151,#1858,.T.);
#3939=EDGE_CURVE('',#3153,#3154,#1859,.T.);
#3940=EDGE_CURVE('',#3154,#3152,#1860,.T.);
#3941=EDGE_CURVE('',#3144,#3153,#1861,.T.);
#3942=EDGE_CURVE('',#3146,#3154,#1862,.T.);
#3943=EDGE_CURVE('',#3155,#3155,#2637,.T.);
#3944=EDGE_CURVE('',#3156,#3156,#2638,.T.);
#3945=EDGE_CURVE('',#3156,#3155,#1863,.T.);
#3946=EDGE_CURVE('',#3157,#3157,#2639,.F.);
#3947=EDGE_CURVE('',#3157,#3156,#1864,.T.);
#3948=EDGE_CURVE('',#3158,#3158,#2640,.T.);
#3949=EDGE_CURVE('',#3158,#3157,#1865,.T.);
#5465=ORIENTED_EDGE('',*,*,#3925,.F.);
#5466=ORIENTED_EDGE('',*,*,#3926,.T.);
#5467=ORIENTED_EDGE('',*,*,#3927,.T.);
#5468=ORIENTED_EDGE('',*,*,#3928,.F.);
#5469=ORIENTED_EDGE('',*,*,#3929,.F.);
#5470=ORIENTED_EDGE('',*,*,#3930,.T.);
#5471=ORIENTED_EDGE('',*,*,#3931,.T.);
#5472=ORIENTED_EDGE('',*,*,#3926,.F.);
#5473=ORIENTED_EDGE('',*,*,#3932,.F.);
#5474=ORIENTED_EDGE('',*,*,#3933,.T.);
#5475=ORIENTED_EDGE('',*,*,#3934,.T.);
#5476=ORIENTED_EDGE('',*,*,#3930,.F.);
#5477=ORIENTED_EDGE('',*,*,#3935,.F.);
#5478=ORIENTED_EDGE('',*,*,#3936,.T.);
#5479=ORIENTED_EDGE('',*,*,#3937,.T.);
#5480=ORIENTED_EDGE('',*,*,#3933,.F.);
#5481=ORIENTED_EDGE('',*,*,#3938,.F.);
#5482=ORIENTED_EDGE('',*,*,#3939,.T.);
#5483=ORIENTED_EDGE('',*,*,#3940,.T.);
#5484=ORIENTED_EDGE('',*,*,#3936,.F.);
#5485=ORIENTED_EDGE('',*,*,#3941,.F.);
#5486=ORIENTED_EDGE('',*,*,#3928,.T.);
#5487=ORIENTED_EDGE('',*,*,#3942,.T.);
#5488=ORIENTED_EDGE('',*,*,#3939,.F.);
#5489=ORIENTED_EDGE('',*,*,#3942,.F.);
#5490=ORIENTED_EDGE('',*,*,#3927,.F.);
#5491=ORIENTED_EDGE('',*,*,#3931,.F.);
#5492=ORIENTED_EDGE('',*,*,#3934,.F.);
#5493=ORIENTED_EDGE('',*,*,#3937,.F.);
#5494=ORIENTED_EDGE('',*,*,#3940,.F.);
#5495=ORIENTED_EDGE('',*,*,#3943,.F.);
#5496=ORIENTED_EDGE('',*,*,#3925,.T.);
#5497=ORIENTED_EDGE('',*,*,#3941,.T.);
#5498=ORIENTED_EDGE('',*,*,#3938,.T.);
#5499=ORIENTED_EDGE('',*,*,#3935,.T.);
#5500=ORIENTED_EDGE('',*,*,#3932,.T.);
#5501=ORIENTED_EDGE('',*,*,#3929,.T.);
#5502=ORIENTED_EDGE('',*,*,#3944,.F.);
#5503=ORIENTED_EDGE('',*,*,#3945,.T.);
#5504=ORIENTED_EDGE('',*,*,#3943,.T.);
#5505=ORIENTED_EDGE('',*,*,#3945,.F.);
#5506=ORIENTED_EDGE('',*,*,#3946,.F.);
#5507=ORIENTED_EDGE('',*,*,#3947,.T.);
#5508=ORIENTED_EDGE('',*,*,#3944,.T.);
#5509=ORIENTED_EDGE('',*,*,#3947,.F.);
#5510=ORIENTED_EDGE('',*,*,#3948,.F.);
#5511=ORIENTED_EDGE('',*,*,#3949,.T.);
#5512=ORIENTED_EDGE('',*,*,#3946,.T.);
#5513=ORIENTED_EDGE('',*,*,#3949,.F.);
#5514=ORIENTED_EDGE('',*,*,#3948,.T.);
#5781=CYLINDRICAL_SURFACE('',#7122,0.24505);
#6093=ADVANCED_FACE('',(#982),#645,.F.);
#6094=ADVANCED_FACE('',(#983),#646,.F.);
#6095=ADVANCED_FACE('',(#984),#647,.F.);
#6096=ADVANCED_FACE('',(#985),#648,.F.);
#6097=ADVANCED_FACE('',(#986),#649,.F.);
#6098=ADVANCED_FACE('',(#987),#650,.F.);
#6099=ADVANCED_FACE('',(#988),#651,.F.);
#6100=ADVANCED_FACE('',(#989,#501),#652,.T.);
#6101=ADVANCED_FACE('',(#990),#274,.T.);
#6102=ADVANCED_FACE('',(#991),#5781,.T.);
#6103=ADVANCED_FACE('',(#992),#275,.T.);
#6104=ADVANCED_FACE('',(#993),#653,.T.);
#6157=CLOSED_SHELL('',(#6093,#6094,#6095,#6096,#6097,#6098,#6099,#6100,
#6101,#6102,#6103,#6104));
#7110=AXIS2_PLACEMENT_3D('',#11459,#8876,#8877);
#7111=AXIS2_PLACEMENT_3D('',#11460,#8878,#8879);
#7112=AXIS2_PLACEMENT_3D('',#11469,#8884,#8885);
#7113=AXIS2_PLACEMENT_3D('',#11475,#8889,#8890);
#7114=AXIS2_PLACEMENT_3D('',#11481,#8894,#8895);
#7115=AXIS2_PLACEMENT_3D('',#11487,#8899,#8900);
#7116=AXIS2_PLACEMENT_3D('',#11493,#8904,#8905);
#7117=AXIS2_PLACEMENT_3D('',#11496,#8908,#8909);
#7118=AXIS2_PLACEMENT_3D('',#11497,#8910,#8911);
#7119=AXIS2_PLACEMENT_3D('',#11499,#8912,#8913);
#7120=AXIS2_PLACEMENT_3D('',#11500,#8914,#8915);
#7121=AXIS2_PLACEMENT_3D('',#11502,#8916,#8917);
#7122=AXIS2_PLACEMENT_3D('',#11504,#8919,#8920);
#7123=AXIS2_PLACEMENT_3D('',#11506,#8921,#8922);
#7124=AXIS2_PLACEMENT_3D('',#11508,#8924,#8925);
#7125=AXIS2_PLACEMENT_3D('',#11510,#8926,#8927);
#7126=AXIS2_PLACEMENT_3D('',#11512,#8929,#8930);
#8876=DIRECTION('axis',(0.,0.,1.));
#8877=DIRECTION('refdir',(1.,0.,0.));
#8878=DIRECTION('center_axis',(0.866025403784439,0.,-0.5));
#8879=DIRECTION('ref_axis',(0.5,0.,0.866025403784439));
#8880=DIRECTION('',(0.5,0.,0.866025403784439));
#8881=DIRECTION('',(0.,-1.,0.));
#8882=DIRECTION('',(0.5,0.,0.866025403784439));
#8883=DIRECTION('',(0.,-1.,0.));
#8884=DIRECTION('center_axis',(1.92296268638356E-16,0.,-1.));
#8885=DIRECTION('ref_axis',(1.,0.,1.92296268638356E-16));
#8886=DIRECTION('',(1.,0.,1.92296268638356E-16));
#8887=DIRECTION('',(0.,-1.,0.));
#8888=DIRECTION('',(1.,0.,1.92296268638356E-16));
#8889=DIRECTION('center_axis',(-0.866025403784439,0.,-0.5));
#8890=DIRECTION('ref_axis',(0.5,0.,-0.866025403784439));
#8891=DIRECTION('',(0.5,0.,-0.866025403784439));
#8892=DIRECTION('',(0.,-1.,0.));
#8893=DIRECTION('',(0.5,0.,-0.866025403784438));
#8894=DIRECTION('center_axis',(-0.866025403784439,0.,0.5));
#8895=DIRECTION('ref_axis',(-0.5,0.,-0.866025403784439));
#8896=DIRECTION('',(-0.5,0.,-0.866025403784439));
#8897=DIRECTION('',(0.,-1.,0.));
#8898=DIRECTION('',(-0.5,0.,-0.866025403784439));
#8899=DIRECTION('center_axis',(-1.92296268638356E-16,0.,1.));
#8900=DIRECTION('ref_axis',(-1.,0.,-1.92296268638356E-16));
#8901=DIRECTION('',(-1.,0.,-1.92296268638356E-16));
#8902=DIRECTION('',(0.,-1.,0.));
#8903=DIRECTION('',(-1.,0.,-1.92296268638356E-16));
#8904=DIRECTION('center_axis',(0.866025403784439,0.,0.5));
#8905=DIRECTION('ref_axis',(-0.5,0.,0.866025403784439));
#8906=DIRECTION('',(-0.5,0.,0.866025403784439));
#8907=DIRECTION('',(-0.5,0.,0.866025403784439));
#8908=DIRECTION('center_axis',(0.,-1.,0.));
#8909=DIRECTION('ref_axis',(0.,0.,-1.));
#8910=DIRECTION('center_axis',(0.,1.,0.));
#8911=DIRECTION('ref_axis',(0.,0.,1.));
#8912=DIRECTION('center_axis',(0.,-1.,0.));
#8913=DIRECTION('ref_axis',(1.,0.,0.));
#8914=DIRECTION('center_axis',(0.,-1.,0.));
#8915=DIRECTION('ref_axis',(1.,0.,0.));
#8916=DIRECTION('center_axis',(0.,-1.,0.));
#8917=DIRECTION('ref_axis',(1.,0.,0.));
#8918=DIRECTION('',(0.707106781186547,0.707106781186548,8.65956056235493E-17));
#8919=DIRECTION('center_axis',(0.,-1.,0.));
#8920=DIRECTION('ref_axis',(1.,0.,0.));
#8921=DIRECTION('center_axis',(0.,1.,0.));
#8922=DIRECTION('ref_axis',(1.,0.,0.));
#8923=DIRECTION('',(0.,1.,0.));
#8924=DIRECTION('center_axis',(0.,1.,0.));
#8925=DIRECTION('ref_axis',(1.,0.,0.));
#8926=DIRECTION('center_axis',(0.,-1.,0.));
#8927=DIRECTION('ref_axis',(1.,0.,0.));
#8928=DIRECTION('',(-0.707106781186547,0.707106781186548,-8.65956056235493E-17));
#8929=DIRECTION('center_axis',(0.,-1.,0.));
#8930=DIRECTION('ref_axis',(0.,0.,-1.));
#11459=CARTESIAN_POINT('',(0.,0.,0.));
#11460=CARTESIAN_POINT('Origin',(0.0721687836487032,0.,-0.125));
#11461=CARTESIAN_POINT('',(0.0721687836487032,0.,-0.125));
#11462=CARTESIAN_POINT('',(0.144337567297406,0.,0.));
#11463=CARTESIAN_POINT('',(0.117710979560879,0.,-0.0461186027918559));
#11464=CARTESIAN_POINT('',(0.0721687836487032,-0.25,-0.125));
#11465=CARTESIAN_POINT('',(0.0721687836487032,0.,-0.125));
#11466=CARTESIAN_POINT('',(0.144337567297406,-0.25,0.));
#11467=CARTESIAN_POINT('',(0.144337567297406,-0.25,0.));
#11468=CARTESIAN_POINT('',(0.144337567297406,0.,0.));
#11469=CARTESIAN_POINT('Origin',(-0.0721687836487032,0.,-0.125));
#11470=CARTESIAN_POINT('',(-0.0721687836487032,0.,-0.125));
#11471=CARTESIAN_POINT('',(0.0739156081756484,0.,-0.125));
#11472=CARTESIAN_POINT('',(-0.0721687836487032,-0.25,-0.125));
#11473=CARTESIAN_POINT('',(-0.0721687836487032,0.,-0.125));
#11474=CARTESIAN_POINT('',(0.0721687836487032,-0.25,-0.125));
#11475=CARTESIAN_POINT('Origin',(-0.144337567297406,0.,-4.16333634234434E-17));
#11476=CARTESIAN_POINT('',(-0.144337567297406,0.,-1.76762539787485E-17));
#11477=CARTESIAN_POINT('',(-0.0987953713852306,0.,-0.0788813972081442));
#11478=CARTESIAN_POINT('',(-0.144337567297406,-0.25,-2.77555756156289E-17));
#11479=CARTESIAN_POINT('',(-0.144337567297406,0.,-1.76762539787485E-17));
#11480=CARTESIAN_POINT('',(-0.0721687836487032,-0.25,-0.125));
#11481=CARTESIAN_POINT('Origin',(-0.0721687836487033,0.,0.125));
#11482=CARTESIAN_POINT('',(-0.0721687836487033,0.,0.125));
#11483=CARTESIAN_POINT('',(-0.0627109795608791,0.,0.141381397208144));
#11484=CARTESIAN_POINT('',(-0.0721687836487033,-0.25,0.125));
#11485=CARTESIAN_POINT('',(-0.0721687836487033,0.,0.125));
#11486=CARTESIAN_POINT('',(-0.144337567297406,-0.25,-1.76762539787485E-17));
#11487=CARTESIAN_POINT('Origin',(0.0721687836487032,0.,0.125));
#11488=CARTESIAN_POINT('',(0.0721687836487032,0.,0.125));
#11489=CARTESIAN_POINT('',(0.146084391824352,0.,0.125));
#11490=CARTESIAN_POINT('',(0.0721687836487032,-0.25,0.125));
#11491=CARTESIAN_POINT('',(0.0721687836487032,0.,0.125));
#11492=CARTESIAN_POINT('',(-0.0721687836487033,-0.25,0.125));
#11493=CARTESIAN_POINT('Origin',(0.144337567297406,0.,0.));
#11494=CARTESIAN_POINT('',(0.153795371385231,0.,-0.0163813972081441));
#11495=CARTESIAN_POINT('',(0.0721687836487032,-0.25,0.125));
#11496=CARTESIAN_POINT('Origin',(0.,-0.25,0.));
#11497=CARTESIAN_POINT('Origin',(0.22,0.,0.));
#11498=CARTESIAN_POINT('',(-0.22,-8.67361737988404E-18,-2.69422295812418E-17));
#11499=CARTESIAN_POINT('Origin',(0.,0.,0.));
#11500=CARTESIAN_POINT('Origin',(0.,-0.015,0.));
#11501=CARTESIAN_POINT('',(-0.24505,-0.02505,-3.00099698131059E-17));
#11502=CARTESIAN_POINT('Origin',(0.,-0.02505,0.));
#11503=CARTESIAN_POINT('',(-0.235,-0.015,-2.87791997799628E-17));
#11504=CARTESIAN_POINT('Origin',(0.,-0.3775,0.));
#11505=CARTESIAN_POINT('',(-0.24505,-0.72995,3.00099698131059E-17));
#11506=CARTESIAN_POINT('Origin',(0.,-0.72995,0.));
#11507=CARTESIAN_POINT('',(-0.24505,-0.3775,-3.00099698131059E-17));
#11508=CARTESIAN_POINT('Origin',(0.,-0.7625,0.));
#11509=CARTESIAN_POINT('',(-0.175,-0.8,-2.14313189850787E-17));
#11510=CARTESIAN_POINT('Origin',(0.,-0.8,0.));
#11511=CARTESIAN_POINT('',(-0.2125,-0.7625,-2.60237444818813E-17));
#11512=CARTESIAN_POINT('Origin',(0.,-0.8,0.));
#11728=UNCERTAINTY_MEASURE_WITH_UNIT(LENGTH_MEASURE(0.001),#11765,
'DISTANCE_ACCURACY_VALUE',
'Maximum model space distance between geometric entities at asserted c
onnectivities');
#11732=UNCERTAINTY_MEASURE_WITH_UNIT(LENGTH_MEASURE(0.001),#11765,
'DISTANCE_ACCURACY_VALUE',
'Maximum model space distance between geometric entities at asserted c
onnectivities');
#11760=(
GEOMETRIC_REPRESENTATION_CONTEXT(3)
GLOBAL_UNCERTAINTY_ASSIGNED_CONTEXT((#11728))
GLOBAL_UNIT_ASSIGNED_CONTEXT((#11765,#11767,#11768))
REPRESENTATION_CONTEXT('','3D')
);
#11764=(
GEOMETRIC_REPRESENTATION_CONTEXT(3)
GLOBAL_UNCERTAINTY_ASSIGNED_CONTEXT((#11732))
GLOBAL_UNIT_ASSIGNED_CONTEXT((#11765,#11767,#11768))
REPRESENTATION_CONTEXT('','3D')
);
#11765=(
LENGTH_UNIT()
NAMED_UNIT(*)
SI_UNIT(.CENTI.,.METRE.)
);
#11767=(
NAMED_UNIT(*)
PLANE_ANGLE_UNIT()
SI_UNIT($,.RADIAN.)
);
#11768=(
NAMED_UNIT(*)
SI_UNIT($,.STERADIAN.)
SOLID_ANGLE_UNIT()
);
#11796=SHAPE_DEFINITION_REPRESENTATION(#11829,#11905);
#11829=PRODUCT_DEFINITION_SHAPE('',$,#11937);
#11905=SHAPE_REPRESENTATION('',(#7110),#11760);
#11909=PRODUCT_DEFINITION_CONTEXT('part definition',#12004,'design');
#11937=PRODUCT_DEFINITION('Socket Set Screw - M5x8',
'Socket Set Screw - M5x8',#11968,#11909);
#11968=PRODUCT_DEFINITION_FORMATION('',$,#12033);
#12004=APPLICATION_CONTEXT(
'Core Data for Automotive Mechanical Design Process');
#12005=PRODUCT_CONTEXT('part definition',#12004,'mechanical');
#12033=PRODUCT('Socket Set Screw - M5x8','Socket Set Screw - M5x8',
'Socket Set Screw - M5x8',(#12005));
#12100=COLOUR_RGB('Black',0.12,0.14,0.17);
#12101=FILL_AREA_STYLE_COLOUR('',#12100);
#12102=FILL_AREA_STYLE('',(#12101));
#12103=SURFACE_STYLE_FILL_AREA(#12102);
#12104=SURFACE_SIDE_STYLE('',(#12103));
#12105=SURFACE_STYLE_USAGE(.BOTH.,#12104);
#12106=PRESENTATION_STYLE_ASSIGNMENT((#12105));
ENDSEC;
END-ISO-10303-21;
